ISO-10303-21;
HEADER;
FILE_DESCRIPTION (('STEP AP214'),
    '1' );
FILE_NAME ('slotted cheese head screw_iso_ISO 1207 - M5 x 35 - 35N.step',
    '2026-10-24T22:54:28',
    ( '' ),
    ( '' ),
    'SwSTEP 2.0',
    'SolidWorks 2025',
    '' );
FILE_SCHEMA (( 'AUTOMOTIVE_DESIGN' ));
ENDSEC;

DATA;
#208=CARTESIAN_POINT ( 'NONE',  ( 1.090397816225958216, -0.6000000000000004219, 4.012069227840649788 ) ) ;
#315=EDGE_CURVE ( 'NONE', #9594, #14002, #20041, .T. ) ;
#349=( NAMED_UNIT ( * ) PLANE_ANGLE_UNIT ( ) SI_UNIT ( $, .RADIAN. ) );
#355=AXIS2_PLACEMENT_3D ( 'NONE', #34375, #21798, #3297 ) ;
#378=FACE_OUTER_BOUND ( 'NONE', #3984, .T. ) ;
#399=CARTESIAN_POINT ( 'NONE',  ( 0.000000000000000000, -0.6000000000000003109, 3.730072921939604047 ) ) ;
#441=ORIENTED_EDGE ( 'NONE', *, *, #31035, .T. ) ;
#496=EDGE_CURVE ( 'NONE', #31349, #11061, #19543, .T. ) ;
#550=ORIENTED_EDGE ( 'NONE', *, *, #14859, .T. ) ;
#555=VECTOR ( 'NONE', #26285, 1000.000000000000000 ) ;
#590=ADVANCED_FACE ( 'NONE', ( #35261 ), #24902, .T. ) ;
#754=EDGE_CURVE ( 'NONE', #9594, #8017, #12125, .T. ) ;
#845=AXIS2_PLACEMENT_3D ( 'NONE', #34297, #6066, #28080 ) ;
#957=ORIENTED_EDGE ( 'NONE', *, *, #23789, .T. ) ;
#959=SHAPE_DEFINITION_REPRESENTATION ( #39464, #28236 ) ;
#1012=AXIS2_PLACEMENT_3D ( 'NONE', #16573, #16185, #22383 ) ;
#1064=AXIS2_PLACEMENT_3D ( 'NONE', #40573, #37291, #8465 ) ;
#1078=CARTESIAN_POINT ( 'NONE',  ( 0.3454438073187036107, 0.5999999999999995337, -3.946157045896960369 ) ) ;
#1358=ORIENTED_EDGE ( 'NONE', *, *, #8530, .T. ) ;
#1425=FACE_OUTER_BOUND ( 'NONE', #26472, .T. ) ;
#1561=ORIENTED_EDGE ( 'NONE', *, *, #9680, .F. ) ;
#1618=CARTESIAN_POINT ( 'NONE',  ( 0.1825688514504736626, 0.5999999999999995337, -3.931742364880508767 ) ) ;
#1647=CIRCLE ( 'NONE', #8849, 2.500000000000000000 ) ;
#1735=VERTEX_POINT ( 'NONE', #24502 ) ;
#1868=CARTESIAN_POINT ( 'NONE',  ( 0.000000000000000000, -0.5999999999999994227, -3.730072921939604047 ) ) ;
#2129=VERTEX_POINT ( 'NONE', #27678 ) ;
#2175=FACE_OUTER_BOUND ( 'NONE', #30006, .T. ) ;
#2219=ORIENTED_EDGE ( 'NONE', *, *, #23789, .F. ) ;
#2259=ORIENTED_EDGE ( 'NONE', *, *, #13212, .F. ) ;
#2553=EDGE_CURVE ( 'NONE', #3797, #27685, #19466, .T. ) ;
#2598=( LENGTH_UNIT ( ) NAMED_UNIT ( * ) SI_UNIT ( .MILLI., .METRE. ) );
#2671=CARTESIAN_POINT ( 'NONE',  ( 0.1825688514504806015, 0.5999999999999995337, 3.931742364880953744 ) ) ;
#2781=LINE ( 'NONE', #6053, #36218 ) ;
#3079=CARTESIAN_POINT ( 'NONE',  ( 1.300000000000000044, 0.5999999999999995337, 4.250000000000000000 ) ) ;
#3090=CARTESIAN_POINT ( 'NONE',  ( 1.300000000000000044, 0.5999999999999995337, 4.030609108440248889 ) ) ;
#3099=CARTESIAN_POINT ( 'NONE',  ( 0.1330790777139393422, 0.5999999999999995337, 3.927362444725310819 ) ) ;
#3157=DIRECTION ( 'NONE',  ( 0.000000000000000000, 0.000000000000000000, 1.000000000000000000 ) ) ;
#3297=DIRECTION ( 'NONE',  ( 0.000000000000000000, 0.000000000000000000, 1.000000000000000000 ) ) ;
#3325=CARTESIAN_POINT ( 'NONE',  ( 0.3454438073185458480, -0.6000000000000004219, 3.946157045896946602 ) ) ;
#3416=EDGE_LOOP ( 'NONE', ( #17997, #26723 ) ) ;
#3445=DIRECTION ( 'NONE',  ( 0.000000000000000000, 0.000000000000000000, 1.000000000000000000 ) ) ;
#3481=PLANE ( 'NONE',  #29434 ) ;
#3500=CARTESIAN_POINT ( 'NONE',  ( 0.01899362242916388319, 0.5999999999999995337, 3.829601239880993990 ) ) ;
#3553=DIRECTION ( 'NONE',  ( 1.000000000000000000, 0.000000000000000000, 0.000000000000000000 ) ) ;
#3564=CARTESIAN_POINT ( 'NONE',  ( 0.000000000000000000, -0.6000000000000003109, 3.730072921939604047 ) ) ;
#3619=ADVANCED_FACE ( 'NONE', ( #4724 ), #36028, .F. ) ;
#3656=FACE_OUTER_BOUND ( 'NONE', #39726, .T. ) ;
#3674=LINE ( 'NONE', #6934, #555 ) ;
#3741=ORIENTED_EDGE ( 'NONE', *, *, #18894, .F. ) ;
#3766=CARTESIAN_POINT ( 'NONE',  ( 0.000000000000000000, 0.000000000000000000, 0.000000000000000000 ) ) ;
#3797=VERTEX_POINT ( 'NONE', #399 ) ;
#3806=AXIS2_PLACEMENT_3D ( 'NONE', #5241, #24179, #17989 ) ;
#3834=EDGE_CURVE ( 'NONE', #8999, #14282, #15873, .T. ) ;
#3970=LINE ( 'NONE', #16489, #35145 ) ;
#3984=EDGE_LOOP ( 'NONE', ( #38476, #2259, #7737, #10448, #31005, #957 ) ) ;
#4110=ORIENTED_EDGE ( 'NONE', *, *, #39600, .T. ) ;
#4510=CARTESIAN_POINT ( 'NONE',  ( 0.08557765857971742773, 0.5999999999999995337, -3.903564864120421696 ) ) ;
#4699=CARTESIAN_POINT ( 'NONE',  ( 0.1326080060424829343, 0.5999999999999995337, -3.927320754166761851 ) ) ;
#4724=FACE_OUTER_BOUND ( 'NONE', #13639, .T. ) ;
#4747=CARTESIAN_POINT ( 'NONE',  ( 0.01878240296280925953, -0.5999999999999994227, -3.829296454260694205 ) ) ;
#4748=DIRECTION ( 'NONE',  ( 0.000000000000000000, 0.000000000000000000, -1.000000000000000000 ) ) ;
#4756=CARTESIAN_POINT ( 'NONE',  ( 0.1825688514436868137, -0.5999999999999994227, -3.931742364907163001 ) ) ;
#4781=DIRECTION ( 'NONE',  ( -0.000000000000000000, 0.000000000000000000, 1.000000000000000000 ) ) ;
#4960=CARTESIAN_POINT ( 'NONE',  ( 0.8807958757747544887, -0.5999999999999994227, -3.993526596136941720 ) ) ;
#5008=CARTESIAN_POINT ( 'NONE',  ( 0.000000000000000000, 0.000000000000000000, 0.000000000000000000 ) ) ;
#5043=CIRCLE ( 'NONE', #28055, 2.500000000000000000 ) ;
#5241=CARTESIAN_POINT ( 'NONE',  ( 3.300000000000000266, 2.500000000000000000, 0.000000000000000000 ) ) ;
#5247=( NAMED_UNIT ( * ) SI_UNIT ( $, .STERADIAN. ) SOLID_ANGLE_UNIT ( ) );
#5293=ADVANCED_FACE ( 'NONE', ( #26384 ), #38222, .T. ) ;
#5412=ORIENTED_EDGE ( 'NONE', *, *, #754, .F. ) ;
#5726=LINE ( 'NONE', #11263, #30076 ) ;
#5796=ORIENTED_EDGE ( 'NONE', *, *, #2553, .T. ) ;
#5817=CARTESIAN_POINT ( 'NONE',  ( 0.1825688514500733994, -0.6000000000000004219, 3.931742364882332197 ) ) ;
#5851=DIRECTION ( 'NONE',  ( 0.9961946980917455452, 1.067350013832301366E-17, 0.08715574274765851281 ) ) ;
#6053=CARTESIAN_POINT ( 'NONE',  ( 0.000000000000000000, 4.851177947605531887E-16, 3.961287410364449979 ) ) ;
#6066=DIRECTION ( 'NONE',  ( 1.000000000000000000, -0.000000000000000000, -0.000000000000000000 ) ) ;
#6257=EDGE_CURVE ( 'NONE', #14282, #7409, #3674, .T. ) ;
#6356=CARTESIAN_POINT ( 'NONE',  ( 0.3454438073187346969, 0.5999999999999995337, 3.946157045896963034 ) ) ;
#6537=ORIENTED_EDGE ( 'NONE', *, *, #25890, .F. ) ;
#6581=DIRECTION ( 'NONE',  ( 0.000000000000000000, 0.000000000000000000, 1.000000000000000000 ) ) ;
#6757=ORIENTED_EDGE ( 'NONE', *, *, #36845, .T. ) ;
#6787=CARTESIAN_POINT ( 'NONE',  ( 0.8807958757747548217, -0.6000000000000004219, 3.993526596136941720 ) ) ;
#6834=CARTESIAN_POINT ( 'NONE',  ( 0.5083189215984414977, 0.5999999999999995337, -3.960569937088434411 ) ) ;
#6934=CARTESIAN_POINT ( 'NONE',  ( 0.000000000000000000, 0.5999999999999995337, 4.250000000000000000 ) ) ;
#7139=ORIENTED_EDGE ( 'NONE', *, *, #23382, .F. ) ;
#7237=FACE_OUTER_BOUND ( 'NONE', #37435, .T. ) ;
#7409=VERTEX_POINT ( 'NONE', #20449 ) ;
#7516=PRODUCT_CONTEXT ( 'NONE', #33465, 'mechanical' ) ;
#7737=ORIENTED_EDGE ( 'NONE', *, *, #15538, .T. ) ;
#7751=DIRECTION ( 'NONE',  ( 0.000000000000000000, 0.000000000000000000, 1.000000000000000000 ) ) ;
#7831=CARTESIAN_POINT ( 'NONE',  ( 0.1332591166277097561, -0.5999999999999993117, -3.927378378441396922 ) ) ;
#8017=VERTEX_POINT ( 'NONE', #24933 ) ;
#8030=CARTESIAN_POINT ( 'NONE',  ( 0.5083189215969784458, -0.5999999999999994227, -3.960569937088305181 ) ) ;
#8393=AXIS2_PLACEMENT_3D ( 'NONE', #20093, #16789, #32869 ) ;
#8465=DIRECTION ( 'NONE',  ( 0.000000000000000000, 0.000000000000000000, 1.000000000000000000 ) ) ;
#8523=CIRCLE ( 'NONE', #36142, 4.250000000000000000 ) ;
#8526=VERTEX_POINT ( 'NONE', #19285 ) ;
#8530=EDGE_CURVE ( 'NONE', #19906, #26819, #8523, .T. ) ;
#8849=AXIS2_PLACEMENT_3D ( 'NONE', #38498, #31333, #3157 ) ;
#8999=VERTEX_POINT ( 'NONE', #2671 ) ;
#9159=EDGE_CURVE ( 'NONE', #27685, #14002, #9890, .T. ) ;
#9187=ORIENTED_EDGE ( 'NONE', *, *, #23836, .T. ) ;
#9406=DIRECTION ( 'NONE',  ( 0.000000000000000000, -0.000000000000000000, 1.000000000000000000 ) ) ;
#9416=CARTESIAN_POINT ( 'NONE',  ( 0.5083189215984570408, 0.5999999999999995337, 3.960569937088435299 ) ) ;
#9485=DIRECTION ( 'NONE',  ( 0.000000000000000000, 0.000000000000000000, 1.000000000000000000 ) ) ;
#9594=VERTEX_POINT ( 'NONE', #26454 ) ;
#9627=( GEOMETRIC_REPRESENTATION_CONTEXT ( 3 ) GLOBAL_UNCERTAINTY_ASSIGNED_CONTEXT ( ( #39873 ) ) GLOBAL_UNIT_ASSIGNED_CONTEXT ( ( #2598, #27480, #5247 ) ) REPRESENTATION_CONTEXT ( 'NONE', 'WORKASPACE' ) );
#9680=EDGE_CURVE ( 'NONE', #20773, #19906, #2781, .T. ) ;
#9829=CARTESIAN_POINT ( 'NONE',  ( 3.300000000000000711, 0.000000000000000000, 0.000000000000000000 ) ) ;
#9862=ORIENTED_EDGE ( 'NONE', *, *, #13667, .F. ) ;
#9890=CIRCLE ( 'NONE', #28944, 3.977260115179314770 ) ;
#9957=DIRECTION ( 'NONE',  ( 0.000000000000000000, 8.881784197001253901E-15, 1.000000000000000000 ) ) ;
#10200=ORIENTED_EDGE ( 'NONE', *, *, #36845, .F. ) ;
#10381=DIRECTION ( 'NONE',  ( 0.000000000000000000, 0.000000000000000000, 1.000000000000000000 ) ) ;
#10448=ORIENTED_EDGE ( 'NONE', *, *, #3834, .T. ) ;
#10519=CARTESIAN_POINT ( 'NONE',  ( 0.1825688514500733994, -0.6000000000000004219, 3.931742364882332197 ) ) ;
#10545=PLANE ( 'NONE',  #17325 ) ;
#10586=AXIS2_PLACEMENT_3D ( 'NONE', #5008, #30538, #17539 ) ;
#10683=CIRCLE ( 'NONE', #845, 4.075022672948151126 ) ;
#10757=EDGE_CURVE ( 'NONE', #22478, #3797, #27018, .T. ) ;
#10803=ORIENTED_EDGE ( 'NONE', *, *, #23432, .T. ) ;
#10942=ORIENTED_EDGE ( 'NONE', *, *, #315, .F. ) ;
#11005=( GEOMETRIC_REPRESENTATION_CONTEXT ( 3 ) GLOBAL_UNCERTAINTY_ASSIGNED_CONTEXT ( ( #21353 ) ) GLOBAL_UNIT_ASSIGNED_CONTEXT ( ( #19275, #349, #25655 ) ) REPRESENTATION_CONTEXT ( 'NONE', 'WORKASPACE' ) );
#11010=PLANE ( 'NONE',  #8393 ) ;
#11044=VERTEX_POINT ( 'NONE', #13734 ) ;
#11061=VERTEX_POINT ( 'NONE', #26297 ) ;
#11263=CARTESIAN_POINT ( 'NONE',  ( 0.000000000000000000, -0.5999999999999994227, -4.250000000000000000 ) ) ;
#11379=DIRECTION ( 'NONE',  ( -1.000000000000000000, -0.000000000000000000, -0.000000000000000000 ) ) ;
#11427=CARTESIAN_POINT ( 'NONE',  ( 0.1825688514504736348, 0.000000000000000000, 0.000000000000000000 ) ) ;
#11474=EDGE_LOOP ( 'NONE', ( #22917, #6757 ) ) ;
#11673=CARTESIAN_POINT ( 'NONE',  ( 1.300000000000000044, 4.990463472878845329E-16, 4.075022672948151126 ) ) ;
#11965=B_SPLINE_CURVE_WITH_KNOTS ( 'NONE', 3,
 ( #31097, #3325, #28612, #28401, #6787, #208, #24706 ),
 .UNSPECIFIED., .F., .F.,
 ( 4, 3, 4 ),
 ( 0.006904927062941951937, 0.007395461772899652141, 0.008026723377514808841 ),
 .UNSPECIFIED. ) ;
#12016=ORIENTED_EDGE ( 'NONE', *, *, #315, .T. ) ;
#12125=LINE ( 'NONE', #34813, #15728 ) ;
#12141=DIRECTION ( 'NONE',  ( 0.000000000000000000, 0.000000000000000000, 1.000000000000000000 ) ) ;
#12326=ORIENTED_EDGE ( 'NONE', *, *, #14859, .F. ) ;
#12410=ADVANCED_FACE ( 'NONE', ( #40206 ), #12789, .T. ) ;
#12667=VECTOR ( 'NONE', #40574, 1000.000000000000000 ) ;
#12789=TOROIDAL_SURFACE ( 'NONE', #22690, 3.778021175560965172, 0.2000000000000000111 ) ;
#12852=CIRCLE ( 'NONE', #26031, 4.075022672948151126 ) ;
#12894=EDGE_LOOP ( 'NONE', ( #2219, #23507, #26684, #12326 ) ) ;
#13005=CARTESIAN_POINT ( 'NONE',  ( 3.811648262644349985E-18, -0.6000000000000000888, 3.780227049350623147 ) ) ;
#13152=CARTESIAN_POINT ( 'NONE',  ( 3.300000000000000711, 0.000000000000000000, 0.000000000000000000 ) ) ;
#13212=EDGE_CURVE ( 'NONE', #1735, #11061, #33348, .T. ) ;
#13235=ORIENTED_EDGE ( 'NONE', *, *, #18894, .T. ) ;
#13246=CARTESIAN_POINT ( 'NONE',  ( 1.300000000000000044, 0.000000000000000000, 0.000000000000000000 ) ) ;
#13304=VERTEX_POINT ( 'NONE', #20972 ) ;
#13480=CIRCLE ( 'NONE', #1012, 3.778021175560965172 ) ;
#13490=ADVANCED_FACE ( 'NONE', ( #31474 ), #31677, .T. ) ;
#13533=DIRECTION ( 'NONE',  ( 1.000000000000000000, -0.000000000000000000, -0.000000000000000000 ) ) ;
#13588=ORIENTED_EDGE ( 'NONE', *, *, #754, .T. ) ;
#13610=CARTESIAN_POINT ( 'NONE',  ( 0.1825688514504736626, 0.5999999999999995337, -3.931742364880508767 ) ) ;
#13639=EDGE_LOOP ( 'NONE', ( #12016, #10803, #441, #5796, #19222, #5412 ) ) ;
#13667=EDGE_CURVE ( 'NONE', #1735, #20773, #12852, .T. ) ;
#13734=CARTESIAN_POINT ( 'NONE',  ( 3.300000000000000711, 0.000000000000000000, 2.500000000000000000 ) ) ;
#13915=FACE_OUTER_BOUND ( 'NONE', #27861, .T. ) ;
#13927=PLANE ( 'NONE',  #30494 ) ;
#14002=VERTEX_POINT ( 'NONE', #33547 ) ;
#14027=VECTOR ( 'NONE', #24023, 1000.000000000000000 ) ;
#14195=AXIS2_PLACEMENT_3D ( 'NONE', #13152, #31491, #6581 ) ;
#14206=DIRECTION ( 'NONE',  ( 1.000000000000000000, 0.000000000000000000, 0.000000000000000000 ) ) ;
#14251=ORIENTED_EDGE ( 'NONE', *, *, #496, .F. ) ;
#14282=VERTEX_POINT ( 'NONE', #25289 ) ;
#14352=DIRECTION ( 'NONE',  ( 1.000000000000000000, 0.000000000000000000, 0.000000000000000000 ) ) ;
#14667=CONICAL_SURFACE ( 'NONE', #38362, 3.961287410364449979, 0.08726646259971682085 ) ;
#14674=DIRECTION ( 'NONE',  ( 0.000000000000000000, 0.000000000000000000, 1.000000000000000000 ) ) ;
#14859=EDGE_CURVE ( 'NONE', #31349, #8999, #30462, .T. ) ;
#15195=B_SPLINE_CURVE_WITH_KNOTS ( 'NONE', 3,
 ( #3090, #22005, #25088, #37617, #9416, #6356, #15817 ),
 .UNSPECIFIED., .F., .F.,
 ( 4, 3, 4 ),
 ( 0.006764200096651864190, 0.007395461704374725088, 0.007885996417619594440 ),
 .UNSPECIFIED. ) ;
#15343=CARTESIAN_POINT ( 'NONE',  ( 0.1825688514504736348, 0.000000000000000000, 0.000000000000000000 ) ) ;
#15405=CARTESIAN_POINT ( 'NONE',  ( 0.08532122990943709351, 0.5999999999999996447, 3.903274794823348159 ) ) ;
#15476=CARTESIAN_POINT ( 'NONE',  ( 0.01877809797159043712, -0.6000000000000005329, 3.829374602102926239 ) ) ;
#15538=EDGE_CURVE ( 'NONE', #1735, #8999, #15195, .T. ) ;
#15618=ADVANCED_FACE ( 'NONE', ( #26303 ), #13927, .T. ) ;
#15728=VECTOR ( 'NONE', #25115, 1000.000000000000000 ) ;
#15783=SHAPE_REPRESENTATION_RELATIONSHIP ( 'NONE' , 'NONE' ,  #28236, #17103 ) ;
#15817=CARTESIAN_POINT ( 'NONE',  ( 0.1825688514504806015, 0.5999999999999995337, 3.931742364880953744 ) ) ;
#15873=B_SPLINE_CURVE_WITH_KNOTS ( 'NONE', 3,
 ( #25303, #3099, #15405, #3500, #37838, #34992 ),
 .UNSPECIFIED., .F., .F.,
 ( 4, 2, 4 ),
 ( 0.0006940092137399027188, 0.0008426799592462289306, 0.0009913507047525551424 ),
 .UNSPECIFIED. ) ;
#16124=AXIS2_PLACEMENT_3D ( 'NONE', #27900, #22159, #3445 ) ;
#16185=DIRECTION ( 'NONE',  ( -1.000000000000000000, -0.000000000000000000, -0.000000000000000000 ) ) ;
#16364=ADVANCED_FACE ( 'NONE', ( #16522 ), #10545, .T. ) ;
#16489=CARTESIAN_POINT ( 'NONE',  ( -25.39999999999996305, 0.000000000000000000, 2.500000000000000000 ) ) ;
#16490=CARTESIAN_POINT ( 'NONE',  ( 1.090397816225957328, 0.5999999999999995337, -4.012069227840649788 ) ) ;
#16522=FACE_OUTER_BOUND ( 'NONE', #3416, .T. ) ;
#16573=CARTESIAN_POINT ( 'NONE',  ( 0.000000000000000000, 0.000000000000000000, 0.000000000000000000 ) ) ;
#16583=APPLICATION_CONTEXT ( 'automotive_design' ) ;
#16789=DIRECTION ( 'NONE',  ( -1.000000000000000000, 0.000000000000000000, -0.000000000000000000 ) ) ;
#16860=DIRECTION ( 'NONE',  ( 0.000000000000000000, -1.000000000000000000, -1.147978770867004622E-16 ) ) ;
#17004=DIRECTION ( 'NONE',  ( 1.000000000000000000, 0.000000000000000000, 0.000000000000000000 ) ) ;
#17083=CARTESIAN_POINT ( 'NONE',  ( 0.08527861205520151366, -0.5999999999999994227, -3.903297362784067470 ) ) ;
#17085=DIRECTION ( 'NONE',  ( -1.000000000000000000, -0.000000000000000000, -0.000000000000000000 ) ) ;
#17103=ADVANCED_BREP_SHAPE_REPRESENTATION ( '', ( #39462, #30744 ), #11005 ) ;
#17325=AXIS2_PLACEMENT_3D ( 'NONE', #20219, #23523, #4781 ) ;
#17358=ORIENTED_EDGE ( 'NONE', *, *, #25890, .T. ) ;
#17539=DIRECTION ( 'NONE',  ( 0.000000000000000000, 0.000000000000000000, 1.000000000000000000 ) ) ;
#17740=ORIENTED_EDGE ( 'NONE', *, *, #9159, .F. ) ;
#17989=DIRECTION ( 'NONE',  ( -0.000000000000000000, 0.000000000000000000, 1.000000000000000000 ) ) ;
#17997=ORIENTED_EDGE ( 'NONE', *, *, #6257, .F. ) ;
#18189=EDGE_LOOP ( 'NONE', ( #37760, #17740, #18395, #19878 ) ) ;
#18252=ORIENTED_EDGE ( 'NONE', *, *, #31035, .F. ) ;
#18395=ORIENTED_EDGE ( 'NONE', *, *, #2553, .F. ) ;
#18399=EDGE_CURVE ( 'NONE', #20773, #8017, #35910, .T. ) ;
#18481=ORIENTED_EDGE ( 'NONE', *, *, #23836, .F. ) ;
#18684=EDGE_CURVE ( 'NONE', #11044, #2129, #26697, .T. ) ;
#18894=EDGE_CURVE ( 'NONE', #13304, #8526, #38528, .T. ) ;
#19033=DIRECTION ( 'NONE',  ( 1.000000000000000000, -0.000000000000000000, -0.000000000000000000 ) ) ;
#19157=PRODUCT ( 'slotted cheese head screw_iso_ISO 1207 - M5 x 35 - 35N', 'slotted cheese head screw_iso_ISO 1207 - M5 x 35 - 35N', '', ( #7516 ) ) ;
#19186=CARTESIAN_POINT ( 'NONE',  ( 0.08558287364504800487, -0.6000000000000004219, 3.903552650893701514 ) ) ;
#19222=ORIENTED_EDGE ( 'NONE', *, *, #37881, .T. ) ;
#19275=( LENGTH_UNIT ( ) NAMED_UNIT ( * ) SI_UNIT ( .MILLI., .METRE. ) );
#19285=CARTESIAN_POINT ( 'NONE',  ( 38.29999999999999716, 0.000000000000000000, 2.500000000000000000 ) ) ;
#19466=B_SPLINE_CURVE_WITH_KNOTS ( 'NONE', 3,
 ( #3564, #13005, #15476, #19186, #28038, #5817 ),
 .UNSPECIFIED., .F., .F.,
 ( 4, 2, 4 ),
 ( 0.0002675702395149656557, 0.0004161762349008431153, 0.0005647822302867205749 ),
 .UNSPECIFIED. ) ;
#19543=B_SPLINE_CURVE_WITH_KNOTS ( 'NONE', 3,
 ( #13610, #1078, #6834, #38311, #38716, #16490, #28862 ),
 .UNSPECIFIED., .F., .F.,
 ( 4, 3, 4 ),
 ( 0.006904927062942190462, 0.007395461772899653008, 0.008026723377514808841 ),
 .UNSPECIFIED. ) ;
#19800=CYLINDRICAL_SURFACE ( 'NONE', #26734, 2.500000000000000000 ) ;
#19878=ORIENTED_EDGE ( 'NONE', *, *, #10757, .F. ) ;
#19906=VERTEX_POINT ( 'NONE', #25227 ) ;
#20041=B_SPLINE_CURVE_WITH_KNOTS ( 'NONE', 3,
 ( #27180, #36452, #4960, #35864, #8030, #32971, #4756 ),
 .UNSPECIFIED., .F., .F.,
 ( 4, 3, 4 ),
 ( 0.006764200096651864190, 0.007395461704374725088, 0.007885996417624047475 ),
 .UNSPECIFIED. ) ;
#20093=CARTESIAN_POINT ( 'NONE',  ( -1.238631071793920509E-17, 0.000000000000000000, 0.000000000000000000 ) ) ;
#20219=CARTESIAN_POINT ( 'NONE',  ( -1.238631071793920509E-17, 0.000000000000000000, 0.000000000000000000 ) ) ;
#20288=CLOSED_SHELL ( 'NONE', ( #23755, #36569, #16364, #12410, #13490, #22873, #31635, #590, #40530, #5293, #31195, #3619, #15618 ) ) ;
#20422=ORIENTED_EDGE ( 'NONE', *, *, #28504, .T. ) ;
#20449=CARTESIAN_POINT ( 'NONE',  ( 0.000000000000000000, 0.5999999999999995337, -3.730072921939604047 ) ) ;
#20747=DIRECTION ( 'NONE',  ( 0.000000000000000000, -1.147978770867004622E-16, 1.000000000000000000 ) ) ;
#20773=VERTEX_POINT ( 'NONE', #11673 ) ;
#20843=AXIS2_PLACEMENT_3D ( 'NONE', #38782, #38576, #10381 ) ;
#20972=CARTESIAN_POINT ( 'NONE',  ( 38.29999999999999716, 3.061616997868383141E-16, -2.500000000000000000 ) ) ;
#21353=UNCERTAINTY_MEASURE_WITH_UNIT (LENGTH_MEASURE( 1.000000000000000082E-05 ), #19275, 'distance_accuracy_value', 'NONE');
#21459=LINE ( 'NONE', #34438, #12667 ) ;
#21798=DIRECTION ( 'NONE',  ( -1.000000000000000000, -0.000000000000000000, -0.000000000000000000 ) ) ;
#21921=AXIS2_PLACEMENT_3D ( 'NONE', #15343, #27899, #29135 ) ;
#22005=CARTESIAN_POINT ( 'NONE',  ( 1.090397816225957550, 0.5999999999999995337, 4.012069227840649788 ) ) ;
#22159=DIRECTION ( 'NONE',  ( -1.000000000000000000, -0.000000000000000000, -0.000000000000000000 ) ) ;
#22167=CIRCLE ( 'NONE', #33323, 4.075022672948151126 ) ;
#22326=CARTESIAN_POINT ( 'NONE',  ( 3.300000000000000711, 0.000000000000000000, -4.250000000000000000 ) ) ;
#22375=EDGE_CURVE ( 'NONE', #8526, #13304, #1647, .T. ) ;
#22383=DIRECTION ( 'NONE',  ( 0.000000000000000000, 0.000000000000000000, 1.000000000000000000 ) ) ;
#22478=VERTEX_POINT ( 'NONE', #1868 ) ;
#22590=DIRECTION ( 'NONE',  ( 0.000000000000000000, 0.000000000000000000, 1.000000000000000000 ) ) ;
#22690=AXIS2_PLACEMENT_3D ( 'NONE', #36318, #11379, #14674 ) ;
#22784=PLANE ( 'NONE',  #33870 ) ;
#22862=PRODUCT_DEFINITION_FORMATION_WITH_SPECIFIED_SOURCE ( 'ANY', '', #19157, .NOT_KNOWN. ) ;
#22864=CARTESIAN_POINT ( 'NONE',  ( 1.300000000000000044, -0.5999999999999994227, -4.250000000000000000 ) ) ;
#22873=ADVANCED_FACE ( 'NONE', ( #3656 ), #22784, .T. ) ;
#22914=EDGE_CURVE ( 'NONE', #14282, #7409, #13480, .T. ) ;
#22917=ORIENTED_EDGE ( 'NONE', *, *, #18684, .T. ) ;
#23097=CARTESIAN_POINT ( 'NONE',  ( -25.39999999999996305, 0.000000000000000000, 0.000000000000000000 ) ) ;
#23148=ORIENTED_EDGE ( 'NONE', *, *, #37881, .F. ) ;
#23265=DIRECTION ( 'NONE',  ( 0.000000000000000000, 1.147978770867004622E-16, -1.000000000000000000 ) ) ;
#23286=CARTESIAN_POINT ( 'NONE',  ( 0.2000000000000000111, 0.000000000000000000, 0.000000000000000000 ) ) ;
#23382=EDGE_CURVE ( 'NONE', #8526, #11044, #3970, .T. ) ;
#23432=EDGE_CURVE ( 'NONE', #14002, #22478, #34709, .T. ) ;
#23507=ORIENTED_EDGE ( 'NONE', *, *, #22914, .F. ) ;
#23523=DIRECTION ( 'NONE',  ( -1.000000000000000000, 0.000000000000000000, -0.000000000000000000 ) ) ;
#23628=LINE ( 'NONE', #36192, #14027 ) ;
#23755=ADVANCED_FACE ( 'NONE', ( #1425 ), #14667, .T. ) ;
#23789=EDGE_CURVE ( 'NONE', #7409, #31349, #40562, .T. ) ;
#23791=DIRECTION ( 'NONE',  ( 0.000000000000000000, 0.000000000000000000, 1.000000000000000000 ) ) ;
#23836=EDGE_CURVE ( 'NONE', #38454, #26819, #23628, .T. ) ;
#24023=DIRECTION ( 'NONE',  ( 0.9961946980917455452, 0.000000000000000000, -0.08715574274765851281 ) ) ;
#24179=DIRECTION ( 'NONE',  ( -1.000000000000000000, 0.000000000000000000, -0.000000000000000000 ) ) ;
#24194=ORIENTED_EDGE ( 'NONE', *, *, #8530, .F. ) ;
#24502=CARTESIAN_POINT ( 'NONE',  ( 1.300000000000000044, 0.5999999999999995337, 4.030609108440248889 ) ) ;
#24706=CARTESIAN_POINT ( 'NONE',  ( 1.300000000000000044, -0.6000000000000003109, 4.030609108440248889 ) ) ;
#24902=CONICAL_SURFACE ( 'NONE', #30845, 3.961287410364449979, 0.08726646259971682085 ) ;
#24933=CARTESIAN_POINT ( 'NONE',  ( 1.300000000000000044, -0.6000000000000003109, 4.030609108440248889 ) ) ;
#25088=CARTESIAN_POINT ( 'NONE',  ( 0.8807958757747544887, 0.5999999999999995337, 3.993526596136941720 ) ) ;
#25115=DIRECTION ( 'NONE',  ( 0.000000000000000000, -1.147978770867004622E-16, 1.000000000000000000 ) ) ;
#25227=CARTESIAN_POINT ( 'NONE',  ( 3.300000000000000711, 5.204748896376251685E-16, 4.250000000000000000 ) ) ;
#25289=CARTESIAN_POINT ( 'NONE',  ( 0.000000000000000000, 0.5999999999999995337, 3.730072921939604047 ) ) ;
#25303=CARTESIAN_POINT ( 'NONE',  ( 0.1825688514504806015, 0.5999999999999995337, 3.931742364880953744 ) ) ;
#25537=EDGE_CURVE ( 'NONE', #38454, #11061, #10683, .T. ) ;
#25655=( NAMED_UNIT ( * ) SI_UNIT ( $, .STERADIAN. ) SOLID_ANGLE_UNIT ( ) );
#25665=DIRECTION ( 'NONE',  ( -1.000000000000000000, -0.000000000000000000, -0.000000000000000000 ) ) ;
#25890=EDGE_CURVE ( 'NONE', #13304, #2129, #21459, .T. ) ;
#25958=ORIENTED_EDGE ( 'NONE', *, *, #25537, .T. ) ;
#26031=AXIS2_PLACEMENT_3D ( 'NONE', #35776, #13533, #34986 ) ;
#26190=DIRECTION ( 'NONE',  ( 0.000000000000000000, 0.000000000000000000, 1.000000000000000000 ) ) ;
#26285=DIRECTION ( 'NONE',  ( 0.000000000000000000, 0.000000000000000000, -1.000000000000000000 ) ) ;
#26297=CARTESIAN_POINT ( 'NONE',  ( 1.300000000000000044, 0.5999999999999995337, -4.030609108440248889 ) ) ;
#26303=FACE_OUTER_BOUND ( 'NONE', #28954, .T. ) ;
#26384=FACE_OUTER_BOUND ( 'NONE', #18189, .T. ) ;
#26454=CARTESIAN_POINT ( 'NONE',  ( 1.300000000000000044, -0.5999999999999994227, -4.030609108440248889 ) ) ;
#26472=EDGE_LOOP ( 'NONE', ( #39106, #35039, #1358, #18481, #25958, #14251, #550, #35845 ) ) ;
#26546=DIRECTION ( 'NONE',  ( 0.000000000000000000, 0.000000000000000000, -1.000000000000000000 ) ) ;
#26684=ORIENTED_EDGE ( 'NONE', *, *, #3834, .F. ) ;
#26697=CIRCLE ( 'NONE', #14195, 2.500000000000000000 ) ;
#26723=ORIENTED_EDGE ( 'NONE', *, *, #22914, .T. ) ;
#26734=AXIS2_PLACEMENT_3D ( 'NONE', #23097, #35664, #26190 ) ;
#26779=CARTESIAN_POINT ( 'NONE',  ( 0.000000000000000000, -0.5999999999999994227, -3.730072921939604047 ) ) ;
#26819=VERTEX_POINT ( 'NONE', #22326 ) ;
#27018=CIRCLE ( 'NONE', #10586, 3.778021175560965172 ) ;
#27180=CARTESIAN_POINT ( 'NONE',  ( 1.300000000000000044, -0.5999999999999994227, -4.030609108440248889 ) ) ;
#27480=( NAMED_UNIT ( * ) PLANE_ANGLE_UNIT ( ) SI_UNIT ( $, .RADIAN. ) );
#27678=CARTESIAN_POINT ( 'NONE',  ( 3.300000000000000711, 3.061616997868383141E-16, -2.500000000000000000 ) ) ;
#27685=VERTEX_POINT ( 'NONE', #10519 ) ;
#27745=ORIENTED_EDGE ( 'NONE', *, *, #28504, .F. ) ;
#27861=EDGE_LOOP ( 'NONE', ( #18252, #33936 ) ) ;
#27899=DIRECTION ( 'NONE',  ( 1.000000000000000000, 0.000000000000000000, 0.000000000000000000 ) ) ;
#27900=CARTESIAN_POINT ( 'NONE',  ( 38.29999999999999716, 0.000000000000000000, 0.000000000000000000 ) ) ;
#28038=CARTESIAN_POINT ( 'NONE',  ( 0.1331427388959149360, -0.6000000000000004219, 3.927368078836517729 ) ) ;
#28055=AXIS2_PLACEMENT_3D ( 'NONE', #9829, #38027, #12141 ) ;
#28080=DIRECTION ( 'NONE',  ( 0.000000000000000000, 0.000000000000000000, 1.000000000000000000 ) ) ;
#28236=SHAPE_REPRESENTATION ( 'slotted cheese head screw_iso_ISO 1207 - M5 x 35 - 35N', ( #30744 ), #11005 ) ;
#28401=CARTESIAN_POINT ( 'NONE',  ( 0.6711941891205337463, -0.6000000000000004219, 3.974981096219152299 ) ) ;
#28504=EDGE_CURVE ( 'NONE', #26819, #19906, #34049, .T. ) ;
#28612=CARTESIAN_POINT ( 'NONE',  ( 0.5083189215983626719, -0.6000000000000004219, 3.960569937088427306 ) ) ;
#28862=CARTESIAN_POINT ( 'NONE',  ( 1.300000000000000044, 0.5999999999999995337, -4.030609108440248889 ) ) ;
#28944=AXIS2_PLACEMENT_3D ( 'NONE', #11427, #17004, #23791 ) ;
#28954=EDGE_LOOP ( 'NONE', ( #13588, #30210, #9862, #36183, #40592, #37535 ) ) ;
#29063=DIRECTION ( 'NONE',  ( -1.000000000000000000, -0.000000000000000000, -0.000000000000000000 ) ) ;
#29135=DIRECTION ( 'NONE',  ( 0.000000000000000000, 0.000000000000000000, 1.000000000000000000 ) ) ;
#29386=DIRECTION ( 'NONE',  ( -1.000000000000000000, 0.000000000000000000, 0.000000000000000000 ) ) ;
#29434=AXIS2_PLACEMENT_3D ( 'NONE', #3079, #34974, #9406 ) ;
#29677=AXIS2_PLACEMENT_3D ( 'NONE', #23286, #17085, #38717 ) ;
#30006=EDGE_LOOP ( 'NONE', ( #27745, #24194 ) ) ;
#30076=VECTOR ( 'NONE', #20747, 1000.000000000000000 ) ;
#30198=ORIENTED_EDGE ( 'NONE', *, *, #9159, .T. ) ;
#30210=ORIENTED_EDGE ( 'NONE', *, *, #18399, .F. ) ;
#30424=CARTESIAN_POINT ( 'NONE',  ( 0.01871827436868165120, 0.5999999999999996447, -3.829290154341121966 ) ) ;
#30462=CIRCLE ( 'NONE', #21921, 3.977260115179314770 ) ;
#30494=AXIS2_PLACEMENT_3D ( 'NONE', #32481, #29386, #7751 ) ;
#30538=DIRECTION ( 'NONE',  ( -1.000000000000000000, -0.000000000000000000, -0.000000000000000000 ) ) ;
#30744=AXIS2_PLACEMENT_3D ( 'NONE', #35448, #9485, #3553 ) ;
#30845=AXIS2_PLACEMENT_3D ( 'NONE', #3766, #14206, #4748 ) ;
#30853=CARTESIAN_POINT ( 'NONE',  ( 0.1825688514504736626, 0.5999999999999995337, -3.931742364880508767 ) ) ;
#30937=ORIENTED_EDGE ( 'NONE', *, *, #18399, .T. ) ;
#31005=ORIENTED_EDGE ( 'NONE', *, *, #6257, .T. ) ;
#31035=EDGE_CURVE ( 'NONE', #22478, #3797, #5726, .T. ) ;
#31097=CARTESIAN_POINT ( 'NONE',  ( 0.1825688514500733994, -0.6000000000000004219, 3.931742364882332197 ) ) ;
#31195=ADVANCED_FACE ( 'NONE', ( #378 ), #3481, .F. ) ;
#31257=ORIENTED_EDGE ( 'NONE', *, *, #18684, .F. ) ;
#31327=STYLED_ITEM('',(#40766),#39462);
#31333=DIRECTION ( 'NONE',  ( -1.000000000000000000, -0.000000000000000000, -0.000000000000000000 ) ) ;
#31349=VERTEX_POINT ( 'NONE', #30853 ) ;
#31474=FACE_OUTER_BOUND ( 'NONE', #38417, .T. ) ;
#31491=DIRECTION ( 'NONE',  ( -1.000000000000000000, -0.000000000000000000, -0.000000000000000000 ) ) ;
#31635=ADVANCED_FACE ( 'NONE', ( #13915 ), #11010, .T. ) ;
#31677=CYLINDRICAL_SURFACE ( 'NONE', #355, 2.500000000000000000 ) ;
#31851=CARTESIAN_POINT ( 'NONE',  ( 3.300000000000000711, 0.000000000000000000, 0.000000000000000000 ) ) ;
#32444=CARTESIAN_POINT ( 'NONE',  ( 1.300000000000000044, 0.000000000000000000, -4.075022672948151126 ) ) ;
#32481=CARTESIAN_POINT ( 'NONE',  ( 1.300000000000000044, 0.5999999999999995337, -4.250000000000000000 ) ) ;
#32869=DIRECTION ( 'NONE',  ( -0.000000000000000000, 0.000000000000000000, 1.000000000000000000 ) ) ;
#32971=CARTESIAN_POINT ( 'NONE',  ( 0.3454438073157775624, -0.5999999999999994227, -3.946157045896701021 ) ) ;
#33323=AXIS2_PLACEMENT_3D ( 'NONE', #13246, #19033, #9957 ) ;
#33348=LINE ( 'NONE', #33748, #37152 ) ;
#33465=APPLICATION_CONTEXT ( 'automotive_design' ) ;
#33531=CARTESIAN_POINT ( 'NONE',  ( 0.000000000000000000, 0.5999999999999995337, -3.730072921939604047 ) ) ;
#33547=CARTESIAN_POINT ( 'NONE',  ( 0.1825688514436868137, -0.5999999999999994227, -3.931742364907163001 ) ) ;
#33748=CARTESIAN_POINT ( 'NONE',  ( 1.300000000000000044, 0.5999999999999995337, 4.250000000000000000 ) ) ;
#33781=CARTESIAN_POINT ( 'NONE',  ( 0.1825688514436868137, -0.5999999999999994227, -3.931742364907163001 ) ) ;
#33870=AXIS2_PLACEMENT_3D ( 'NONE', #38603, #34948, #38806 ) ;
#33936=ORIENTED_EDGE ( 'NONE', *, *, #10757, .T. ) ;
#34049=CIRCLE ( 'NONE', #20843, 4.250000000000000000 ) ;
#34106=ORIENTED_EDGE ( 'NONE', *, *, #22375, .F. ) ;
#34297=CARTESIAN_POINT ( 'NONE',  ( 1.300000000000000044, 0.000000000000000000, 0.000000000000000000 ) ) ;
#34375=CARTESIAN_POINT ( 'NONE',  ( -25.39999999999996305, 0.000000000000000000, 0.000000000000000000 ) ) ;
#34438=CARTESIAN_POINT ( 'NONE',  ( -25.39999999999996305, 3.061616997868383141E-16, -2.500000000000000000 ) ) ;
#34709=B_SPLINE_CURVE_WITH_KNOTS ( 'NONE', 3,
 ( #33781, #7831, #17083, #4747, #36053, #26779 ),
 .UNSPECIFIED., .F., .F.,
 ( 4, 2, 4 ),
 ( 0.001123090053775944184, 0.001271523439455638860, 0.001419956825135333537 ),
 .UNSPECIFIED. ) ;
#34813=CARTESIAN_POINT ( 'NONE',  ( 1.300000000000000044, -0.5999999999999994227, -4.250000000000000000 ) ) ;
#34948=DIRECTION ( 'NONE',  ( 1.000000000000000000, 0.000000000000000000, 0.000000000000000000 ) ) ;
#34974=DIRECTION ( 'NONE',  ( 0.000000000000000000, 1.000000000000000000, 0.000000000000000000 ) ) ;
#34986=DIRECTION ( 'NONE',  ( 0.000000000000000000, -1.332267629550187849E-14, 1.000000000000000000 ) ) ;
#34992=CARTESIAN_POINT ( 'NONE',  ( 0.000000000000000000, 0.5999999999999995337, 3.730072921939604047 ) ) ;
#35039=ORIENTED_EDGE ( 'NONE', *, *, #9680, .T. ) ;
#35145=VECTOR ( 'NONE', #29063, 1000.000000000000000 ) ;
#35261=FACE_OUTER_BOUND ( 'NONE', #36949, .T. ) ;
#35448=CARTESIAN_POINT ( 'NONE',  ( 0.000000000000000000, 0.000000000000000000, 0.000000000000000000 ) ) ;
#35664=DIRECTION ( 'NONE',  ( -1.000000000000000000, -0.000000000000000000, -0.000000000000000000 ) ) ;
#35776=CARTESIAN_POINT ( 'NONE',  ( 1.300000000000000044, 0.000000000000000000, 0.000000000000000000 ) ) ;
#35845=ORIENTED_EDGE ( 'NONE', *, *, #15538, .F. ) ;
#35864=CARTESIAN_POINT ( 'NONE',  ( 0.6711941891205337463, -0.5999999999999994227, -3.974981096219152299 ) ) ;
#35910=CIRCLE ( 'NONE', #1064, 4.075022672948151126 ) ;
#36028=PLANE ( 'NONE',  #37484 ) ;
#36053=CARTESIAN_POINT ( 'NONE',  ( -4.547719893808338520E-15, -0.5999999999999994227, -3.779600343874077062 ) ) ;
#36142=AXIS2_PLACEMENT_3D ( 'NONE', #31851, #25665, #22590 ) ;
#36183=ORIENTED_EDGE ( 'NONE', *, *, #13212, .T. ) ;
#36192=CARTESIAN_POINT ( 'NONE',  ( 0.000000000000000000, 0.000000000000000000, -3.961287410364449979 ) ) ;
#36218=VECTOR ( 'NONE', #5851, 1000.000000000000000 ) ;
#36222=ORIENTED_EDGE ( 'NONE', *, *, #23382, .T. ) ;
#36318=CARTESIAN_POINT ( 'NONE',  ( 0.2000000000000000111, 0.000000000000000000, 0.000000000000000000 ) ) ;
#36452=CARTESIAN_POINT ( 'NONE',  ( 1.090397816225957550, -0.5999999999999994227, -4.012069227840649788 ) ) ;
#36566=MECHANICAL_DESIGN_GEOMETRIC_PRESENTATION_REPRESENTATION('',(#31327),#9627);
#36569=ADVANCED_FACE ( 'NONE', ( #7237 ), #19800, .T. ) ;
#36836=ORIENTED_EDGE ( 'NONE', *, *, #22375, .T. ) ;
#36845=EDGE_CURVE ( 'NONE', #2129, #11044, #5043, .T. ) ;
#36949=EDGE_LOOP ( 'NONE', ( #1561, #30937, #23148, #30198, #10942, #4110, #9187, #20422 ) ) ;
#37152=VECTOR ( 'NONE', #26546, 1000.000000000000000 ) ;
#37291=DIRECTION ( 'NONE',  ( 1.000000000000000000, -0.000000000000000000, -0.000000000000000000 ) ) ;
#37435=EDGE_LOOP ( 'NONE', ( #36836, #17358, #31257, #7139 ) ) ;
#37484=AXIS2_PLACEMENT_3D ( 'NONE', #22864, #16860, #23265 ) ;
#37535=ORIENTED_EDGE ( 'NONE', *, *, #39600, .F. ) ;
#37617=CARTESIAN_POINT ( 'NONE',  ( 0.6711941891205337463, 0.5999999999999995337, 3.974981096219152299 ) ) ;
#37760=ORIENTED_EDGE ( 'NONE', *, *, #23432, .F. ) ;
#37838=CARTESIAN_POINT ( 'NONE',  ( -3.676122991083663472E-15, 0.5999999999999995337, 3.779754562795982764 ) ) ;
#37881=EDGE_CURVE ( 'NONE', #27685, #8017, #11965, .T. ) ;
#38027=DIRECTION ( 'NONE',  ( -1.000000000000000000, -0.000000000000000000, -0.000000000000000000 ) ) ;
#38222=TOROIDAL_SURFACE ( 'NONE', #29677, 3.778021175560965172, 0.2000000000000000111 ) ;
#38311=CARTESIAN_POINT ( 'NONE',  ( 0.6711941891205335242, 0.5999999999999995337, -3.974981096219152299 ) ) ;
#38362=AXIS2_PLACEMENT_3D ( 'NONE', #39059, #14352, #39672 ) ;
#38417=EDGE_LOOP ( 'NONE', ( #6537, #13235, #36222, #10200 ) ) ;
#38454=VERTEX_POINT ( 'NONE', #32444 ) ;
#38476=ORIENTED_EDGE ( 'NONE', *, *, #496, .T. ) ;
#38498=CARTESIAN_POINT ( 'NONE',  ( 38.29999999999999716, 0.000000000000000000, 0.000000000000000000 ) ) ;
#38528=CIRCLE ( 'NONE', #16124, 2.500000000000000000 ) ;
#38576=DIRECTION ( 'NONE',  ( -1.000000000000000000, -0.000000000000000000, -0.000000000000000000 ) ) ;
#38603=CARTESIAN_POINT ( 'NONE',  ( 38.29999999999999716, 2.500000000000000000, 0.000000000000000000 ) ) ;
#38716=CARTESIAN_POINT ( 'NONE',  ( 0.8807958757747543777, 0.5999999999999995337, -3.993526596136941720 ) ) ;
#38717=DIRECTION ( 'NONE',  ( 0.000000000000000000, 0.000000000000000000, 1.000000000000000000 ) ) ;
#38782=CARTESIAN_POINT ( 'NONE',  ( 3.300000000000000711, 0.000000000000000000, 0.000000000000000000 ) ) ;
#38806=DIRECTION ( 'NONE',  ( 0.000000000000000000, 0.000000000000000000, -1.000000000000000000 ) ) ;
#39059=CARTESIAN_POINT ( 'NONE',  ( 0.000000000000000000, 0.000000000000000000, 0.000000000000000000 ) ) ;
#39106=ORIENTED_EDGE ( 'NONE', *, *, #13667, .T. ) ;
#39264=CARTESIAN_POINT ( 'NONE',  ( -4.108956827130609367E-15, 0.5999999999999995337, -3.779699080088179564 ) ) ;
#39396=PRODUCT_DEFINITION ( 'UNKNOWN', '', #22862, #39452 ) ;
#39403=PLANE ( 'NONE',  #3806 ) ;
#39452=PRODUCT_DEFINITION_CONTEXT ( 'detailed design', #16583, 'design' ) ;
#39462=MANIFOLD_SOLID_BREP ( 'Slot', #20288 ) ;
#39464=PRODUCT_DEFINITION_SHAPE ( 'NONE', 'NONE',  #39396 ) ;
#39600=EDGE_CURVE ( 'NONE', #9594, #38454, #22167, .T. ) ;
#39672=DIRECTION ( 'NONE',  ( 0.000000000000000000, 0.000000000000000000, -1.000000000000000000 ) ) ;
#39726=EDGE_LOOP ( 'NONE', ( #34106, #3741 ) ) ;
#39829=FACE_BOUND ( 'NONE', #11474, .T. ) ;
#39873=UNCERTAINTY_MEASURE_WITH_UNIT (LENGTH_MEASURE( 1.000000000000000082E-05 ), #2598, 'distance_accuracy_value', 'NONE');
#40206=FACE_OUTER_BOUND ( 'NONE', #12894, .T. ) ;
#40530=ADVANCED_FACE ( 'NONE', ( #2175, #39829 ), #39403, .F. ) ;
#40562=B_SPLINE_CURVE_WITH_KNOTS ( 'NONE', 3,
 ( #33531, #39264, #30424, #4510, #4699, #1618 ),
 .UNSPECIFIED., .F., .F.,
 ( 4, 2, 4 ),
 ( 0.001097151095971008686, 0.001245689619143885377, 0.001394228142316762285 ),
 .UNSPECIFIED. ) ;
#40573=CARTESIAN_POINT ( 'NONE',  ( 1.300000000000000044, 0.000000000000000000, 0.000000000000000000 ) ) ;
#40574=DIRECTION ( 'NONE',  ( -1.000000000000000000, -0.000000000000000000, -0.000000000000000000 ) ) ;
#40592=ORIENTED_EDGE ( 'NONE', *, *, #25537, .F. ) ;
#40760=COLOUR_RGB('Black',0.12,0.14,0.17);
#40761=FILL_AREA_STYLE_COLOUR('',#40760);
#40762=FILL_AREA_STYLE('',(#40761));
#40763=SURFACE_STYLE_FILL_AREA(#40762);
#40764=SURFACE_SIDE_STYLE('',(#40763));
#40765=SURFACE_STYLE_USAGE(.BOTH.,#40764);
#40766=PRESENTATION_STYLE_ASSIGNMENT((#40765));
ENDSEC;
END-ISO-10303-21;
